ISO-10303-21;
HEADER;
/* Generated by software containing ST-Developer
 * from STEP Tools, Inc. (www.steptools.com) 
 */

FILE_DESCRIPTION(
/* description */ (''),
/* implementation_level */ '2;1');

FILE_NAME(
/* name */ 'Middle_Block_02.step',
/* time_stamp */ '2026-10-23T22:30:33+06:00',
/* author */ (''),
/* organization */ (''),
/* preprocessor_version */ 'ST-DEVELOPER v20.2',
/* originating_system */ 'Autodesk Translation Framework v15.15.0.0',
/* authorisation */ '');

FILE_SCHEMA (('AUTOMOTIVE_DESIGN { 1 0 10303 214 3 1 1 }'));
ENDSEC;

DATA;
#10=MECHANICAL_DESIGN_GEOMETRIC_PRESENTATION_REPRESENTATION('',(#243),#10131);
#159=ELLIPSE('',#6488,1.0823922002924,1.);
#160=ELLIPSE('',#6489,1.08239220029239,1.);
#161=ELLIPSE('',#6491,1.08239220029239,1.);
#162=ELLIPSE('',#6492,1.0823922002924,1.);
#163=ELLIPSE('',#6494,1.0823922002924,1.);
#164=ELLIPSE('',#6496,1.0823922002924,1.);
#165=ELLIPSE('',#6497,1.0823922002924,1.);
#166=ELLIPSE('',#6499,1.08239220029239,1.);
#167=ELLIPSE('',#6502,1.08239220029239,1.);
#168=ELLIPSE('',#6504,1.0823922002924,1.);
#169=ELLIPSE('',#6507,1.08239220029239,1.);
#170=ELLIPSE('',#6509,1.0823922002924,1.);
#171=ELLIPSE('',#6519,1.08239220029239,1.);
#172=ELLIPSE('',#6520,1.08239220029239,1.);
#173=ELLIPSE('',#6522,1.08239220029239,1.);
#174=ELLIPSE('',#6524,1.08239220029239,1.);
#175=ELLIPSE('',#6526,1.08239220029239,1.);
#176=ELLIPSE('',#6528,1.08239220029239,1.);
#177=ELLIPSE('',#6530,1.0823922002924,1.);
#178=ELLIPSE('',#6532,1.08239220029239,1.);
#179=ELLIPSE('',#6534,1.08239220029239,1.);
#180=ELLIPSE('',#6536,1.0823922002924,1.);
#181=ELLIPSE('',#6538,1.0823922002924,1.);
#182=ELLIPSE('',#6540,1.08239220029239,1.);
#223=SHAPE_REPRESENTATION_RELATIONSHIP('SRR','None',#10177,#233);
#233=ADVANCED_BREP_SHAPE_REPRESENTATION('',(#253),#10129);
#243=STYLED_ITEM('',(#10247),#253);
#253=MANIFOLD_SOLID_BREP('Middle_Block_02',#5887);
#316=FACE_BOUND('',#1169,.T.);
#317=FACE_BOUND('',#1170,.T.);
#318=FACE_BOUND('',#1171,.T.);
#319=FACE_BOUND('',#1172,.T.);
#320=FACE_BOUND('',#1188,.T.);
#321=FACE_BOUND('',#1189,.T.);
#322=FACE_BOUND('',#1190,.T.);
#323=FACE_BOUND('',#1191,.T.);
#439=PLANE('',#6511);
#440=PLANE('',#6512);
#441=PLANE('',#6513);
#442=PLANE('',#6514);
#443=PLANE('',#6515);
#444=PLANE('',#6516);
#445=PLANE('',#6517);
#446=PLANE('',#6542);
#447=PLANE('',#6543);
#448=PLANE('',#6544);
#449=PLANE('',#6545);
#450=PLANE('',#6546);
#451=PLANE('',#6547);
#452=PLANE('',#6548);
#736=FACE_OUTER_BOUND('',#1146,.T.);
#737=FACE_OUTER_BOUND('',#1147,.T.);
#738=FACE_OUTER_BOUND('',#1148,.T.);
#739=FACE_OUTER_BOUND('',#1149,.T.);
#740=FACE_OUTER_BOUND('',#1150,.T.);
#741=FACE_OUTER_BOUND('',#1151,.T.);
#742=FACE_OUTER_BOUND('',#1152,.T.);
#743=FACE_OUTER_BOUND('',#1153,.T.);
#744=FACE_OUTER_BOUND('',#1154,.T.);
#745=FACE_OUTER_BOUND('',#1155,.T.);
#746=FACE_OUTER_BOUND('',#1156,.T.);
#747=FACE_OUTER_BOUND('',#1157,.T.);
#748=FACE_OUTER_BOUND('',#1158,.T.);
#749=FACE_OUTER_BOUND('',#1159,.T.);
#750=FACE_OUTER_BOUND('',#1160,.T.);
#751=FACE_OUTER_BOUND('',#1161,.T.);
#752=FACE_OUTER_BOUND('',#1162,.T.);
#753=FACE_OUTER_BOUND('',#1163,.T.);
#754=FACE_OUTER_BOUND('',#1164,.T.);
#755=FACE_OUTER_BOUND('',#1165,.T.);
#756=FACE_OUTER_BOUND('',#1166,.T.);
#757=FACE_OUTER_BOUND('',#1167,.T.);
#758=FACE_OUTER_BOUND('',#1168,.T.);
#759=FACE_OUTER_BOUND('',#1173,.T.);
#760=FACE_OUTER_BOUND('',#1174,.T.);
#761=FACE_OUTER_BOUND('',#1175,.T.);
#762=FACE_OUTER_BOUND('',#1176,.T.);
#763=FACE_OUTER_BOUND('',#1177,.T.);
#764=FACE_OUTER_BOUND('',#1178,.T.);
#765=FACE_OUTER_BOUND('',#1179,.T.);
#766=FACE_OUTER_BOUND('',#1180,.T.);
#767=FACE_OUTER_BOUND('',#1181,.T.);
#768=FACE_OUTER_BOUND('',#1182,.T.);
#769=FACE_OUTER_BOUND('',#1183,.T.);
#770=FACE_OUTER_BOUND('',#1184,.T.);
#771=FACE_OUTER_BOUND('',#1185,.T.);
#772=FACE_OUTER_BOUND('',#1186,.T.);
#773=FACE_OUTER_BOUND('',#1187,.T.);
#774=FACE_OUTER_BOUND('',#1192,.T.);
#775=FACE_OUTER_BOUND('',#1193,.T.);
#776=FACE_OUTER_BOUND('',#1194,.T.);
#777=FACE_OUTER_BOUND('',#1195,.T.);
#1146=EDGE_LOOP('',(#4968,#4969,#4970,#4971));
#1147=EDGE_LOOP('',(#4972,#4973,#4974,#4975));
#1148=EDGE_LOOP('',(#4976,#4977,#4978,#4979));
#1149=EDGE_LOOP('',(#4980,#4981,#4982,#4983));
#1150=EDGE_LOOP('',(#4984,#4985,#4986,#4987));
#1151=EDGE_LOOP('',(#4988,#4989,#4990,#4991));
#1152=EDGE_LOOP('',(#4992,#4993,#4994,#4995));
#1153=EDGE_LOOP('',(#4996,#4997,#4998,#4999));
#1154=EDGE_LOOP('',(#5000,#5001,#5002,#5003));
#1155=EDGE_LOOP('',(#5004,#5005,#5006,#5007));
#1156=EDGE_LOOP('',(#5008,#5009,#5010,#5011));
#1157=EDGE_LOOP('',(#5012,#5013,#5014,#5015));
#1158=EDGE_LOOP('',(#5016,#5017,#5018,#5019));
#1159=EDGE_LOOP('',(#5020,#5021,#5022,#5023));
#1160=EDGE_LOOP('',(#5024,#5025,#5026,#5027));
#1161=EDGE_LOOP('',(#5028,#5029,#5030,#5031));
#1162=EDGE_LOOP('',(#5032,#5033,#5034,#5035));
#1163=EDGE_LOOP('',(#5036,#5037,#5038,#5039));
#1164=EDGE_LOOP('',(#5040,#5041,#5042,#5043));
#1165=EDGE_LOOP('',(#5044,#5045,#5046,#5047));
#1166=EDGE_LOOP('',(#5048,#5049,#5050,#5051));
#1167=EDGE_LOOP('',(#5052,#5053,#5054,#5055));
#1168=EDGE_LOOP('',(#5056,#5057,#5058,#5059,#5060,#5061,#5062,#5063,#5064,
#5065,#5066,#5067));
#1169=EDGE_LOOP('',(#5068));
#1170=EDGE_LOOP('',(#5069));
#1171=EDGE_LOOP('',(#5070));
#1172=EDGE_LOOP('',(#5071));
#1173=EDGE_LOOP('',(#5072,#5073,#5074,#5075));
#1174=EDGE_LOOP('',(#5076,#5077,#5078,#5079));
#1175=EDGE_LOOP('',(#5080,#5081,#5082,#5083));
#1176=EDGE_LOOP('',(#5084,#5085,#5086,#5087));
#1177=EDGE_LOOP('',(#5088,#5089,#5090,#5091));
#1178=EDGE_LOOP('',(#5092,#5093,#5094,#5095));
#1179=EDGE_LOOP('',(#5096,#5097,#5098,#5099));
#1180=EDGE_LOOP('',(#5100,#5101,#5102,#5103));
#1181=EDGE_LOOP('',(#5104,#5105,#5106,#5107));
#1182=EDGE_LOOP('',(#5108,#5109,#5110,#5111));
#1183=EDGE_LOOP('',(#5112,#5113,#5114,#5115));
#1184=EDGE_LOOP('',(#5116,#5117,#5118,#5119));
#1185=EDGE_LOOP('',(#5120,#5121,#5122,#5123));
#1186=EDGE_LOOP('',(#5124,#5125,#5126,#5127));
#1187=EDGE_LOOP('',(#5128,#5129,#5130,#5131,#5132,#5133,#5134,#5135,#5136,
#5137,#5138,#5139));
#1188=EDGE_LOOP('',(#5140));
#1189=EDGE_LOOP('',(#5141));
#1190=EDGE_LOOP('',(#5142));
#1191=EDGE_LOOP('',(#5143));
#1192=EDGE_LOOP('',(#5144,#5145,#5146,#5147));
#1193=EDGE_LOOP('',(#5148,#5149,#5150,#5151));
#1194=EDGE_LOOP('',(#5152,#5153,#5154,#5155));
#1195=EDGE_LOOP('',(#5156,#5157,#5158,#5159));
#1660=LINE('',#9737,#2210);
#1661=LINE('',#9743,#2211);
#1662=LINE('',#9749,#2212);
#1663=LINE('',#9755,#2213);
#1664=LINE('',#9760,#2214);
#1665=LINE('',#9764,#2215);
#1666=LINE('',#9769,#2216);
#1667=LINE('',#9773,#2217);
#1668=LINE('',#9777,#2218);
#1669=LINE('',#9780,#2219);
#1670=LINE('',#9784,#2220);
#1671=LINE('',#9788,#2221);
#1672=LINE('',#9792,#2222);
#1673=LINE('',#9795,#2223);
#1674=LINE('',#9797,#2224);
#1675=LINE('',#9798,#2225);
#1676=LINE('',#9801,#2226);
#1677=LINE('',#9803,#2227);
#1678=LINE('',#9807,#2228);
#1679=LINE('',#9809,#2229);
#1680=LINE('',#9812,#2230);
#1681=LINE('',#9813,#2231);
#1682=LINE('',#9816,#2232);
#1683=LINE('',#9818,#2233);
#1684=LINE('',#9822,#2234);
#1685=LINE('',#9824,#2235);
#1686=LINE('',#9827,#2236);
#1687=LINE('',#9828,#2237);
#1688=LINE('',#9831,#2238);
#1689=LINE('',#9833,#2239);
#1690=LINE('',#9834,#2240);
#1691=LINE('',#9837,#2241);
#1692=LINE('',#9838,#2242);
#1693=LINE('',#9841,#2243);
#1694=LINE('',#9842,#2244);
#1695=LINE('',#9845,#2245);
#1696=LINE('',#9846,#2246);
#1697=LINE('',#9849,#2247);
#1698=LINE('',#9850,#2248);
#1699=LINE('',#9853,#2249);
#1700=LINE('',#9854,#2250);
#1701=LINE('',#9859,#2251);
#1702=LINE('',#9863,#2252);
#1703=LINE('',#9867,#2253);
#1704=LINE('',#9870,#2254);
#1705=LINE('',#9873,#2255);
#1706=LINE('',#9876,#2256);
#1707=LINE('',#9879,#2257);
#1708=LINE('',#9882,#2258);
#1709=LINE('',#9885,#2259);
#1710=LINE('',#9887,#2260);
#1711=LINE('',#9890,#2261);
#1712=LINE('',#9894,#2262);
#1713=LINE('',#9898,#2263);
#1714=LINE('',#9902,#2264);
#1715=LINE('',#9906,#2265);
#1716=LINE('',#9910,#2266);
#1717=LINE('',#9913,#2267);
#1718=LINE('',#9914,#2268);
#1719=LINE('',#9916,#2269);
#1720=LINE('',#9918,#2270);
#1721=LINE('',#9921,#2271);
#1722=LINE('',#9923,#2272);
#1723=LINE('',#9925,#2273);
#2210=VECTOR('',#8002,3.);
#2211=VECTOR('',#8009,3.);
#2212=VECTOR('',#8016,3.);
#2213=VECTOR('',#8023,3.);
#2214=VECTOR('',#8028,10.);
#2215=VECTOR('',#8031,10.);
#2216=VECTOR('',#8036,10.);
#2217=VECTOR('',#8039,10.);
#2218=VECTOR('',#8044,10.);
#2219=VECTOR('',#8047,10.);
#2220=VECTOR('',#8050,10.);
#2221=VECTOR('',#8053,10.);
#2222=VECTOR('',#8058,10.);
#2223=VECTOR('',#8061,10.);
#2224=VECTOR('',#8064,10.);
#2225=VECTOR('',#8065,10.);
#2226=VECTOR('',#8068,10.);
#2227=VECTOR('',#8069,10.);
#2228=VECTOR('',#8074,10.);
#2229=VECTOR('',#8075,10.);
#2230=VECTOR('',#8080,10.);
#2231=VECTOR('',#8081,10.);
#2232=VECTOR('',#8084,10.);
#2233=VECTOR('',#8085,10.);
#2234=VECTOR('',#8090,10.);
#2235=VECTOR('',#8091,10.);
#2236=VECTOR('',#8096,10.);
#2237=VECTOR('',#8097,10.);
#2238=VECTOR('',#8100,10.);
#2239=VECTOR('',#8101,10.);
#2240=VECTOR('',#8102,10.);
#2241=VECTOR('',#8105,10.);
#2242=VECTOR('',#8106,10.);
#2243=VECTOR('',#8109,10.);
#2244=VECTOR('',#8110,10.);
#2245=VECTOR('',#8113,10.);
#2246=VECTOR('',#8114,10.);
#2247=VECTOR('',#8117,10.);
#2248=VECTOR('',#8118,10.);
#2249=VECTOR('',#8121,10.);
#2250=VECTOR('',#8122,10.);
#2251=VECTOR('',#8127,10.);
#2252=VECTOR('',#8130,10.);
#2253=VECTOR('',#8135,10.);
#2254=VECTOR('',#8138,10.);
#2255=VECTOR('',#8141,10.);
#2256=VECTOR('',#8144,10.);
#2257=VECTOR('',#8147,10.);
#2258=VECTOR('',#8150,10.);
#2259=VECTOR('',#8153,10.);
#2260=VECTOR('',#8156,10.);
#2261=VECTOR('',#8159,10.);
#2262=VECTOR('',#8164,10.);
#2263=VECTOR('',#8169,10.);
#2264=VECTOR('',#8174,10.);
#2265=VECTOR('',#8179,10.);
#2266=VECTOR('',#8184,10.);
#2267=VECTOR('',#8189,10.);
#2268=VECTOR('',#8190,10.);
#2269=VECTOR('',#8193,10.);
#2270=VECTOR('',#8196,10.);
#2271=VECTOR('',#8201,10.);
#2272=VECTOR('',#8204,10.);
#2273=VECTOR('',#8207,10.);
#2422=CIRCLE('',#6476,3.);
#2423=CIRCLE('',#6477,3.);
#2424=CIRCLE('',#6479,3.);
#2425=CIRCLE('',#6480,3.);
#2426=CIRCLE('',#6482,3.);
#2427=CIRCLE('',#6483,3.);
#2428=CIRCLE('',#6485,3.);
#2429=CIRCLE('',#6486,3.);
#2806=VERTEX_POINT('',#9734);
#2807=VERTEX_POINT('',#9736);
#2808=VERTEX_POINT('',#9740);
#2809=VERTEX_POINT('',#9742);
#2810=VERTEX_POINT('',#9746);
#2811=VERTEX_POINT('',#9748);
#2812=VERTEX_POINT('',#9752);
#2813=VERTEX_POINT('',#9754);
#2814=VERTEX_POINT('',#9758);
#2815=VERTEX_POINT('',#9759);
#2816=VERTEX_POINT('',#9761);
#2817=VERTEX_POINT('',#9763);
#2818=VERTEX_POINT('',#9767);
#2819=VERTEX_POINT('',#9768);
#2820=VERTEX_POINT('',#9770);
#2821=VERTEX_POINT('',#9772);
#2822=VERTEX_POINT('',#9776);
#2823=VERTEX_POINT('',#9778);
#2824=VERTEX_POINT('',#9782);
#2825=VERTEX_POINT('',#9783);
#2826=VERTEX_POINT('',#9785);
#2827=VERTEX_POINT('',#9787);
#2828=VERTEX_POINT('',#9791);
#2829=VERTEX_POINT('',#9793);
#2830=VERTEX_POINT('',#9800);
#2831=VERTEX_POINT('',#9802);
#2832=VERTEX_POINT('',#9806);
#2833=VERTEX_POINT('',#9808);
#2834=VERTEX_POINT('',#9815);
#2835=VERTEX_POINT('',#9817);
#2836=VERTEX_POINT('',#9821);
#2837=VERTEX_POINT('',#9823);
#2838=VERTEX_POINT('',#9830);
#2839=VERTEX_POINT('',#9832);
#2840=VERTEX_POINT('',#9836);
#2841=VERTEX_POINT('',#9840);
#2842=VERTEX_POINT('',#9844);
#2843=VERTEX_POINT('',#9848);
#2844=VERTEX_POINT('',#9852);
#2845=VERTEX_POINT('',#9857);
#2846=VERTEX_POINT('',#9858);
#2847=VERTEX_POINT('',#9860);
#2848=VERTEX_POINT('',#9862);
#2849=VERTEX_POINT('',#9866);
#2850=VERTEX_POINT('',#9868);
#2851=VERTEX_POINT('',#9872);
#2852=VERTEX_POINT('',#9874);
#2853=VERTEX_POINT('',#9878);
#2854=VERTEX_POINT('',#9880);
#2855=VERTEX_POINT('',#9884);
#2856=VERTEX_POINT('',#9889);
#2857=VERTEX_POINT('',#9893);
#2858=VERTEX_POINT('',#9897);
#2859=VERTEX_POINT('',#9901);
#2860=VERTEX_POINT('',#9905);
#2861=VERTEX_POINT('',#9909);
#3536=EDGE_CURVE('',#2806,#2806,#2422,.T.);
#3537=EDGE_CURVE('',#2806,#2807,#1660,.T.);
#3538=EDGE_CURVE('',#2807,#2807,#2423,.T.);
#3539=EDGE_CURVE('',#2808,#2808,#2424,.T.);
#3540=EDGE_CURVE('',#2808,#2809,#1661,.T.);
#3541=EDGE_CURVE('',#2809,#2809,#2425,.T.);
#3542=EDGE_CURVE('',#2810,#2810,#2426,.T.);
#3543=EDGE_CURVE('',#2810,#2811,#1662,.T.);
#3544=EDGE_CURVE('',#2811,#2811,#2427,.T.);
#3545=EDGE_CURVE('',#2812,#2812,#2428,.T.);
#3546=EDGE_CURVE('',#2812,#2813,#1663,.T.);
#3547=EDGE_CURVE('',#2813,#2813,#2429,.T.);
#3548=EDGE_CURVE('',#2814,#2815,#1664,.T.);
#3549=EDGE_CURVE('',#2815,#2816,#159,.T.);
#3550=EDGE_CURVE('',#2816,#2817,#1665,.T.);
#3551=EDGE_CURVE('',#2814,#2817,#160,.T.);
#3552=EDGE_CURVE('',#2818,#2819,#1666,.T.);
#3553=EDGE_CURVE('',#2819,#2820,#161,.T.);
#3554=EDGE_CURVE('',#2820,#2821,#1667,.T.);
#3555=EDGE_CURVE('',#2821,#2818,#162,.T.);
#3556=EDGE_CURVE('',#2819,#2822,#1668,.T.);
#3557=EDGE_CURVE('',#2822,#2823,#163,.T.);
#3558=EDGE_CURVE('',#2823,#2820,#1669,.T.);
#3559=EDGE_CURVE('',#2824,#2825,#1670,.T.);
#3560=EDGE_CURVE('',#2825,#2826,#164,.T.);
#3561=EDGE_CURVE('',#2826,#2827,#1671,.T.);
#3562=EDGE_CURVE('',#2827,#2824,#165,.T.);
#3563=EDGE_CURVE('',#2822,#2828,#1672,.T.);
#3564=EDGE_CURVE('',#2828,#2829,#166,.T.);
#3565=EDGE_CURVE('',#2829,#2823,#1673,.T.);
#3566=EDGE_CURVE('',#2825,#2829,#1674,.T.);
#3567=EDGE_CURVE('',#2828,#2826,#1675,.T.);
#3568=EDGE_CURVE('',#2830,#2824,#1676,.T.);
#3569=EDGE_CURVE('',#2827,#2831,#1677,.T.);
#3570=EDGE_CURVE('',#2831,#2830,#167,.T.);
#3571=EDGE_CURVE('',#2832,#2830,#1678,.T.);
#3572=EDGE_CURVE('',#2831,#2833,#1679,.T.);
#3573=EDGE_CURVE('',#2833,#2832,#168,.T.);
#3574=EDGE_CURVE('',#2815,#2818,#1680,.T.);
#3575=EDGE_CURVE('',#2821,#2816,#1681,.T.);
#3576=EDGE_CURVE('',#2834,#2832,#1682,.T.);
#3577=EDGE_CURVE('',#2833,#2835,#1683,.T.);
#3578=EDGE_CURVE('',#2835,#2834,#169,.T.);
#3579=EDGE_CURVE('',#2836,#2834,#1684,.T.);
#3580=EDGE_CURVE('',#2835,#2837,#1685,.T.);
#3581=EDGE_CURVE('',#2837,#2836,#170,.T.);
#3582=EDGE_CURVE('',#2817,#2836,#1686,.T.);
#3583=EDGE_CURVE('',#2837,#2814,#1687,.T.);
#3584=EDGE_CURVE('',#2821,#2838,#1688,.T.);
#3585=EDGE_CURVE('',#2839,#2838,#1689,.T.);
#3586=EDGE_CURVE('',#2839,#2816,#1690,.T.);
#3587=EDGE_CURVE('',#2820,#2840,#1691,.T.);
#3588=EDGE_CURVE('',#2838,#2840,#1692,.T.);
#3589=EDGE_CURVE('',#2823,#2841,#1693,.T.);
#3590=EDGE_CURVE('',#2840,#2841,#1694,.T.);
#3591=EDGE_CURVE('',#2842,#2829,#1695,.T.);
#3592=EDGE_CURVE('',#2841,#2842,#1696,.T.);
#3593=EDGE_CURVE('',#2825,#2843,#1697,.T.);
#3594=EDGE_CURVE('',#2842,#2843,#1698,.T.);
#3595=EDGE_CURVE('',#2824,#2844,#1699,.T.);
#3596=EDGE_CURVE('',#2843,#2844,#1700,.T.);
#3597=EDGE_CURVE('',#2845,#2846,#1701,.T.);
#3598=EDGE_CURVE('',#2846,#2847,#171,.T.);
#3599=EDGE_CURVE('',#2847,#2848,#1702,.T.);
#3600=EDGE_CURVE('',#2845,#2848,#172,.T.);
#3601=EDGE_CURVE('',#2846,#2849,#1703,.T.);
#3602=EDGE_CURVE('',#2849,#2850,#173,.T.);
#3603=EDGE_CURVE('',#2850,#2847,#1704,.T.);
#3604=EDGE_CURVE('',#2849,#2851,#1705,.T.);
#3605=EDGE_CURVE('',#2851,#2852,#174,.T.);
#3606=EDGE_CURVE('',#2852,#2850,#1706,.T.);
#3607=EDGE_CURVE('',#2851,#2853,#1707,.T.);
#3608=EDGE_CURVE('',#2853,#2854,#175,.T.);
#3609=EDGE_CURVE('',#2854,#2852,#1708,.T.);
#3610=EDGE_CURVE('',#2853,#2855,#1709,.T.);
#3611=EDGE_CURVE('',#2855,#2844,#176,.T.);
#3612=EDGE_CURVE('',#2844,#2854,#1710,.T.);
#3613=EDGE_CURVE('',#2855,#2856,#1711,.T.);
#3614=EDGE_CURVE('',#2856,#2843,#177,.T.);
#3615=EDGE_CURVE('',#2856,#2857,#1712,.T.);
#3616=EDGE_CURVE('',#2857,#2842,#178,.T.);
#3617=EDGE_CURVE('',#2857,#2858,#1713,.T.);
#3618=EDGE_CURVE('',#2858,#2841,#179,.T.);
#3619=EDGE_CURVE('',#2858,#2859,#1714,.T.);
#3620=EDGE_CURVE('',#2859,#2840,#180,.T.);
#3621=EDGE_CURVE('',#2859,#2860,#1715,.T.);
#3622=EDGE_CURVE('',#2860,#2838,#181,.T.);
#3623=EDGE_CURVE('',#2860,#2861,#1716,.T.);
#3624=EDGE_CURVE('',#2861,#2839,#182,.T.);
#3625=EDGE_CURVE('',#2848,#2839,#1717,.T.);
#3626=EDGE_CURVE('',#2861,#2845,#1718,.T.);
#3627=EDGE_CURVE('',#2817,#2848,#1719,.T.);
#3628=EDGE_CURVE('',#2836,#2847,#1720,.T.);
#3629=EDGE_CURVE('',#2834,#2850,#1721,.T.);
#3630=EDGE_CURVE('',#2832,#2852,#1722,.T.);
#3631=EDGE_CURVE('',#2830,#2854,#1723,.T.);
#4968=ORIENTED_EDGE('',*,*,#3536,.F.);
#4969=ORIENTED_EDGE('',*,*,#3537,.T.);
#4970=ORIENTED_EDGE('',*,*,#3538,.F.);
#4971=ORIENTED_EDGE('',*,*,#3537,.F.);
#4972=ORIENTED_EDGE('',*,*,#3539,.F.);
#4973=ORIENTED_EDGE('',*,*,#3540,.T.);
#4974=ORIENTED_EDGE('',*,*,#3541,.F.);
#4975=ORIENTED_EDGE('',*,*,#3540,.F.);
#4976=ORIENTED_EDGE('',*,*,#3542,.F.);
#4977=ORIENTED_EDGE('',*,*,#3543,.T.);
#4978=ORIENTED_EDGE('',*,*,#3544,.F.);
#4979=ORIENTED_EDGE('',*,*,#3543,.F.);
#4980=ORIENTED_EDGE('',*,*,#3545,.F.);
#4981=ORIENTED_EDGE('',*,*,#3546,.T.);
#4982=ORIENTED_EDGE('',*,*,#3547,.F.);
#4983=ORIENTED_EDGE('',*,*,#3546,.F.);
#4984=ORIENTED_EDGE('',*,*,#3548,.T.);
#4985=ORIENTED_EDGE('',*,*,#3549,.T.);
#4986=ORIENTED_EDGE('',*,*,#3550,.T.);
#4987=ORIENTED_EDGE('',*,*,#3551,.F.);
#4988=ORIENTED_EDGE('',*,*,#3552,.T.);
#4989=ORIENTED_EDGE('',*,*,#3553,.T.);
#4990=ORIENTED_EDGE('',*,*,#3554,.T.);
#4991=ORIENTED_EDGE('',*,*,#3555,.T.);
#4992=ORIENTED_EDGE('',*,*,#3556,.T.);
#4993=ORIENTED_EDGE('',*,*,#3557,.T.);
#4994=ORIENTED_EDGE('',*,*,#3558,.T.);
#4995=ORIENTED_EDGE('',*,*,#3553,.F.);
#4996=ORIENTED_EDGE('',*,*,#3559,.T.);
#4997=ORIENTED_EDGE('',*,*,#3560,.T.);
#4998=ORIENTED_EDGE('',*,*,#3561,.T.);
#4999=ORIENTED_EDGE('',*,*,#3562,.T.);
#5000=ORIENTED_EDGE('',*,*,#3563,.T.);
#5001=ORIENTED_EDGE('',*,*,#3564,.T.);
#5002=ORIENTED_EDGE('',*,*,#3565,.T.);
#5003=ORIENTED_EDGE('',*,*,#3557,.F.);
#5004=ORIENTED_EDGE('',*,*,#3566,.T.);
#5005=ORIENTED_EDGE('',*,*,#3564,.F.);
#5006=ORIENTED_EDGE('',*,*,#3567,.T.);
#5007=ORIENTED_EDGE('',*,*,#3560,.F.);
#5008=ORIENTED_EDGE('',*,*,#3568,.T.);
#5009=ORIENTED_EDGE('',*,*,#3562,.F.);
#5010=ORIENTED_EDGE('',*,*,#3569,.T.);
#5011=ORIENTED_EDGE('',*,*,#3570,.T.);
#5012=ORIENTED_EDGE('',*,*,#3571,.T.);
#5013=ORIENTED_EDGE('',*,*,#3570,.F.);
#5014=ORIENTED_EDGE('',*,*,#3572,.T.);
#5015=ORIENTED_EDGE('',*,*,#3573,.T.);
#5016=ORIENTED_EDGE('',*,*,#3574,.T.);
#5017=ORIENTED_EDGE('',*,*,#3555,.F.);
#5018=ORIENTED_EDGE('',*,*,#3575,.T.);
#5019=ORIENTED_EDGE('',*,*,#3549,.F.);
#5020=ORIENTED_EDGE('',*,*,#3576,.T.);
#5021=ORIENTED_EDGE('',*,*,#3573,.F.);
#5022=ORIENTED_EDGE('',*,*,#3577,.T.);
#5023=ORIENTED_EDGE('',*,*,#3578,.T.);
#5024=ORIENTED_EDGE('',*,*,#3579,.T.);
#5025=ORIENTED_EDGE('',*,*,#3578,.F.);
#5026=ORIENTED_EDGE('',*,*,#3580,.T.);
#5027=ORIENTED_EDGE('',*,*,#3581,.T.);
#5028=ORIENTED_EDGE('',*,*,#3582,.T.);
#5029=ORIENTED_EDGE('',*,*,#3581,.F.);
#5030=ORIENTED_EDGE('',*,*,#3583,.T.);
#5031=ORIENTED_EDGE('',*,*,#3551,.T.);
#5032=ORIENTED_EDGE('',*,*,#3575,.F.);
#5033=ORIENTED_EDGE('',*,*,#3584,.T.);
#5034=ORIENTED_EDGE('',*,*,#3585,.F.);
#5035=ORIENTED_EDGE('',*,*,#3586,.T.);
#5036=ORIENTED_EDGE('',*,*,#3554,.F.);
#5037=ORIENTED_EDGE('',*,*,#3587,.T.);
#5038=ORIENTED_EDGE('',*,*,#3588,.F.);
#5039=ORIENTED_EDGE('',*,*,#3584,.F.);
#5040=ORIENTED_EDGE('',*,*,#3558,.F.);
#5041=ORIENTED_EDGE('',*,*,#3589,.T.);
#5042=ORIENTED_EDGE('',*,*,#3590,.F.);
#5043=ORIENTED_EDGE('',*,*,#3587,.F.);
#5044=ORIENTED_EDGE('',*,*,#3565,.F.);
#5045=ORIENTED_EDGE('',*,*,#3591,.F.);
#5046=ORIENTED_EDGE('',*,*,#3592,.F.);
#5047=ORIENTED_EDGE('',*,*,#3589,.F.);
#5048=ORIENTED_EDGE('',*,*,#3566,.F.);
#5049=ORIENTED_EDGE('',*,*,#3593,.T.);
#5050=ORIENTED_EDGE('',*,*,#3594,.F.);
#5051=ORIENTED_EDGE('',*,*,#3591,.T.);
#5052=ORIENTED_EDGE('',*,*,#3559,.F.);
#5053=ORIENTED_EDGE('',*,*,#3595,.T.);
#5054=ORIENTED_EDGE('',*,*,#3596,.F.);
#5055=ORIENTED_EDGE('',*,*,#3593,.F.);
#5056=ORIENTED_EDGE('',*,*,#3561,.F.);
#5057=ORIENTED_EDGE('',*,*,#3567,.F.);
#5058=ORIENTED_EDGE('',*,*,#3563,.F.);
#5059=ORIENTED_EDGE('',*,*,#3556,.F.);
#5060=ORIENTED_EDGE('',*,*,#3552,.F.);
#5061=ORIENTED_EDGE('',*,*,#3574,.F.);
#5062=ORIENTED_EDGE('',*,*,#3548,.F.);
#5063=ORIENTED_EDGE('',*,*,#3583,.F.);
#5064=ORIENTED_EDGE('',*,*,#3580,.F.);
#5065=ORIENTED_EDGE('',*,*,#3577,.F.);
#5066=ORIENTED_EDGE('',*,*,#3572,.F.);
#5067=ORIENTED_EDGE('',*,*,#3569,.F.);
#5068=ORIENTED_EDGE('',*,*,#3538,.T.);
#5069=ORIENTED_EDGE('',*,*,#3541,.T.);
#5070=ORIENTED_EDGE('',*,*,#3544,.T.);
#5071=ORIENTED_EDGE('',*,*,#3547,.T.);
#5072=ORIENTED_EDGE('',*,*,#3597,.T.);
#5073=ORIENTED_EDGE('',*,*,#3598,.T.);
#5074=ORIENTED_EDGE('',*,*,#3599,.T.);
#5075=ORIENTED_EDGE('',*,*,#3600,.F.);
#5076=ORIENTED_EDGE('',*,*,#3601,.T.);
#5077=ORIENTED_EDGE('',*,*,#3602,.T.);
#5078=ORIENTED_EDGE('',*,*,#3603,.T.);
#5079=ORIENTED_EDGE('',*,*,#3598,.F.);
#5080=ORIENTED_EDGE('',*,*,#3604,.T.);
#5081=ORIENTED_EDGE('',*,*,#3605,.T.);
#5082=ORIENTED_EDGE('',*,*,#3606,.T.);
#5083=ORIENTED_EDGE('',*,*,#3602,.F.);
#5084=ORIENTED_EDGE('',*,*,#3607,.T.);
#5085=ORIENTED_EDGE('',*,*,#3608,.T.);
#5086=ORIENTED_EDGE('',*,*,#3609,.T.);
#5087=ORIENTED_EDGE('',*,*,#3605,.F.);
#5088=ORIENTED_EDGE('',*,*,#3610,.T.);
#5089=ORIENTED_EDGE('',*,*,#3611,.T.);
#5090=ORIENTED_EDGE('',*,*,#3612,.T.);
#5091=ORIENTED_EDGE('',*,*,#3608,.F.);
#5092=ORIENTED_EDGE('',*,*,#3613,.T.);
#5093=ORIENTED_EDGE('',*,*,#3614,.T.);
#5094=ORIENTED_EDGE('',*,*,#3596,.T.);
#5095=ORIENTED_EDGE('',*,*,#3611,.F.);
#5096=ORIENTED_EDGE('',*,*,#3594,.T.);
#5097=ORIENTED_EDGE('',*,*,#3614,.F.);
#5098=ORIENTED_EDGE('',*,*,#3615,.T.);
#5099=ORIENTED_EDGE('',*,*,#3616,.T.);
#5100=ORIENTED_EDGE('',*,*,#3592,.T.);
#5101=ORIENTED_EDGE('',*,*,#3616,.F.);
#5102=ORIENTED_EDGE('',*,*,#3617,.T.);
#5103=ORIENTED_EDGE('',*,*,#3618,.T.);
#5104=ORIENTED_EDGE('',*,*,#3590,.T.);
#5105=ORIENTED_EDGE('',*,*,#3618,.F.);
#5106=ORIENTED_EDGE('',*,*,#3619,.T.);
#5107=ORIENTED_EDGE('',*,*,#3620,.T.);
#5108=ORIENTED_EDGE('',*,*,#3588,.T.);
#5109=ORIENTED_EDGE('',*,*,#3620,.F.);
#5110=ORIENTED_EDGE('',*,*,#3621,.T.);
#5111=ORIENTED_EDGE('',*,*,#3622,.T.);
#5112=ORIENTED_EDGE('',*,*,#3585,.T.);
#5113=ORIENTED_EDGE('',*,*,#3622,.F.);
#5114=ORIENTED_EDGE('',*,*,#3623,.T.);
#5115=ORIENTED_EDGE('',*,*,#3624,.T.);
#5116=ORIENTED_EDGE('',*,*,#3625,.T.);
#5117=ORIENTED_EDGE('',*,*,#3624,.F.);
#5118=ORIENTED_EDGE('',*,*,#3626,.T.);
#5119=ORIENTED_EDGE('',*,*,#3600,.T.);
#5120=ORIENTED_EDGE('',*,*,#3550,.F.);
#5121=ORIENTED_EDGE('',*,*,#3586,.F.);
#5122=ORIENTED_EDGE('',*,*,#3625,.F.);
#5123=ORIENTED_EDGE('',*,*,#3627,.F.);
#5124=ORIENTED_EDGE('',*,*,#3582,.F.);
#5125=ORIENTED_EDGE('',*,*,#3627,.T.);
#5126=ORIENTED_EDGE('',*,*,#3599,.F.);
#5127=ORIENTED_EDGE('',*,*,#3628,.F.);
#5128=ORIENTED_EDGE('',*,*,#3597,.F.);
#5129=ORIENTED_EDGE('',*,*,#3626,.F.);
#5130=ORIENTED_EDGE('',*,*,#3623,.F.);
#5131=ORIENTED_EDGE('',*,*,#3621,.F.);
#5132=ORIENTED_EDGE('',*,*,#3619,.F.);
#5133=ORIENTED_EDGE('',*,*,#3617,.F.);
#5134=ORIENTED_EDGE('',*,*,#3615,.F.);
#5135=ORIENTED_EDGE('',*,*,#3613,.F.);
#5136=ORIENTED_EDGE('',*,*,#3610,.F.);
#5137=ORIENTED_EDGE('',*,*,#3607,.F.);
#5138=ORIENTED_EDGE('',*,*,#3604,.F.);
#5139=ORIENTED_EDGE('',*,*,#3601,.F.);
#5140=ORIENTED_EDGE('',*,*,#3536,.T.);
#5141=ORIENTED_EDGE('',*,*,#3539,.T.);
#5142=ORIENTED_EDGE('',*,*,#3542,.T.);
#5143=ORIENTED_EDGE('',*,*,#3545,.T.);
#5144=ORIENTED_EDGE('',*,*,#3579,.F.);
#5145=ORIENTED_EDGE('',*,*,#3628,.T.);
#5146=ORIENTED_EDGE('',*,*,#3603,.F.);
#5147=ORIENTED_EDGE('',*,*,#3629,.F.);
#5148=ORIENTED_EDGE('',*,*,#3576,.F.);
#5149=ORIENTED_EDGE('',*,*,#3629,.T.);
#5150=ORIENTED_EDGE('',*,*,#3606,.F.);
#5151=ORIENTED_EDGE('',*,*,#3630,.F.);
#5152=ORIENTED_EDGE('',*,*,#3571,.F.);
#5153=ORIENTED_EDGE('',*,*,#3630,.T.);
#5154=ORIENTED_EDGE('',*,*,#3609,.F.);
#5155=ORIENTED_EDGE('',*,*,#3631,.F.);
#5156=ORIENTED_EDGE('',*,*,#3568,.F.);
#5157=ORIENTED_EDGE('',*,*,#3631,.T.);
#5158=ORIENTED_EDGE('',*,*,#3612,.F.);
#5159=ORIENTED_EDGE('',*,*,#3595,.F.);
#5478=CYLINDRICAL_SURFACE('',#6475,3.);
#5479=CYLINDRICAL_SURFACE('',#6478,3.);
#5480=CYLINDRICAL_SURFACE('',#6481,3.);
#5481=CYLINDRICAL_SURFACE('',#6484,3.);
#5482=CYLINDRICAL_SURFACE('',#6487,1.);
#5483=CYLINDRICAL_SURFACE('',#6490,1.);
#5484=CYLINDRICAL_SURFACE('',#6493,1.);
#5485=CYLINDRICAL_SURFACE('',#6495,1.);
#5486=CYLINDRICAL_SURFACE('',#6498,1.);
#5487=CYLINDRICAL_SURFACE('',#6500,1.);
#5488=CYLINDRICAL_SURFACE('',#6501,1.);
#5489=CYLINDRICAL_SURFACE('',#6503,1.);
#5490=CYLINDRICAL_SURFACE('',#6505,1.);
#5491=CYLINDRICAL_SURFACE('',#6506,1.);
#5492=CYLINDRICAL_SURFACE('',#6508,1.);
#5493=CYLINDRICAL_SURFACE('',#6510,1.);
#5494=CYLINDRICAL_SURFACE('',#6518,1.);
#5495=CYLINDRICAL_SURFACE('',#6521,1.);
#5496=CYLINDRICAL_SURFACE('',#6523,1.);
#5497=CYLINDRICAL_SURFACE('',#6525,1.);
#5498=CYLINDRICAL_SURFACE('',#6527,1.);
#5499=CYLINDRICAL_SURFACE('',#6529,1.);
#5500=CYLINDRICAL_SURFACE('',#6531,1.);
#5501=CYLINDRICAL_SURFACE('',#6533,1.);
#5502=CYLINDRICAL_SURFACE('',#6535,1.);
#5503=CYLINDRICAL_SURFACE('',#6537,1.);
#5504=CYLINDRICAL_SURFACE('',#6539,1.);
#5505=CYLINDRICAL_SURFACE('',#6541,1.);
#5799=ADVANCED_FACE('',(#736),#5478,.F.);
#5800=ADVANCED_FACE('',(#737),#5479,.F.);
#5801=ADVANCED_FACE('',(#738),#5480,.F.);
#5802=ADVANCED_FACE('',(#739),#5481,.F.);
#5803=ADVANCED_FACE('',(#740),#5482,.T.);
#5804=ADVANCED_FACE('',(#741),#5483,.T.);
#5805=ADVANCED_FACE('',(#742),#5484,.T.);
#5806=ADVANCED_FACE('',(#743),#5485,.T.);
#5807=ADVANCED_FACE('',(#744),#5486,.T.);
#5808=ADVANCED_FACE('',(#745),#5487,.T.);
#5809=ADVANCED_FACE('',(#746),#5488,.T.);
#5810=ADVANCED_FACE('',(#747),#5489,.T.);
#5811=ADVANCED_FACE('',(#748),#5490,.T.);
#5812=ADVANCED_FACE('',(#749),#5491,.T.);
#5813=ADVANCED_FACE('',(#750),#5492,.T.);
#5814=ADVANCED_FACE('',(#751),#5493,.T.);
#5815=ADVANCED_FACE('',(#752),#439,.T.);
#5816=ADVANCED_FACE('',(#753),#440,.T.);
#5817=ADVANCED_FACE('',(#754),#441,.T.);
#5818=ADVANCED_FACE('',(#755),#442,.T.);
#5819=ADVANCED_FACE('',(#756),#443,.T.);
#5820=ADVANCED_FACE('',(#757),#444,.T.);
#5821=ADVANCED_FACE('',(#758,#316,#317,#318,#319),#445,.F.);
#5822=ADVANCED_FACE('',(#759),#5494,.T.);
#5823=ADVANCED_FACE('',(#760),#5495,.T.);
#5824=ADVANCED_FACE('',(#761),#5496,.T.);
#5825=ADVANCED_FACE('',(#762),#5497,.T.);
#5826=ADVANCED_FACE('',(#763),#5498,.T.);
#5827=ADVANCED_FACE('',(#764),#5499,.T.);
#5828=ADVANCED_FACE('',(#765),#5500,.T.);
#5829=ADVANCED_FACE('',(#766),#5501,.T.);
#5830=ADVANCED_FACE('',(#767),#5502,.T.);
#5831=ADVANCED_FACE('',(#768),#5503,.T.);
#5832=ADVANCED_FACE('',(#769),#5504,.T.);
#5833=ADVANCED_FACE('',(#770),#5505,.T.);
#5834=ADVANCED_FACE('',(#771),#446,.T.);
#5835=ADVANCED_FACE('',(#772),#447,.T.);
#5836=ADVANCED_FACE('',(#773,#320,#321,#322,#323),#448,.T.);
#5837=ADVANCED_FACE('',(#774),#449,.T.);
#5838=ADVANCED_FACE('',(#775),#450,.T.);
#5839=ADVANCED_FACE('',(#776),#451,.T.);
#5840=ADVANCED_FACE('',(#777),#452,.T.);
#5887=CLOSED_SHELL('',(#5799,#5800,#5801,#5802,#5803,#5804,#5805,#5806,
#5807,#5808,#5809,#5810,#5811,#5812,#5813,#5814,#5815,#5816,#5817,#5818,
#5819,#5820,#5821,#5822,#5823,#5824,#5825,#5826,#5827,#5828,#5829,#5830,
#5831,#5832,#5833,#5834,#5835,#5836,#5837,#5838,#5839,#5840));
#6474=AXIS2_PLACEMENT_3D('',#9732,#7996,#7997);
#6475=AXIS2_PLACEMENT_3D('',#9733,#7998,#7999);
#6476=AXIS2_PLACEMENT_3D('',#9735,#8000,#8001);
#6477=AXIS2_PLACEMENT_3D('',#9738,#8003,#8004);
#6478=AXIS2_PLACEMENT_3D('',#9739,#8005,#8006);
#6479=AXIS2_PLACEMENT_3D('',#9741,#8007,#8008);
#6480=AXIS2_PLACEMENT_3D('',#9744,#8010,#8011);
#6481=AXIS2_PLACEMENT_3D('',#9745,#8012,#8013);
#6482=AXIS2_PLACEMENT_3D('',#9747,#8014,#8015);
#6483=AXIS2_PLACEMENT_3D('',#9750,#8017,#8018);
#6484=AXIS2_PLACEMENT_3D('',#9751,#8019,#8020);
#6485=AXIS2_PLACEMENT_3D('',#9753,#8021,#8022);
#6486=AXIS2_PLACEMENT_3D('',#9756,#8024,#8025);
#6487=AXIS2_PLACEMENT_3D('',#9757,#8026,#8027);
#6488=AXIS2_PLACEMENT_3D('',#9762,#8029,#8030);
#6489=AXIS2_PLACEMENT_3D('',#9765,#8032,#8033);
#6490=AXIS2_PLACEMENT_3D('',#9766,#8034,#8035);
#6491=AXIS2_PLACEMENT_3D('',#9771,#8037,#8038);
#6492=AXIS2_PLACEMENT_3D('',#9774,#8040,#8041);
#6493=AXIS2_PLACEMENT_3D('',#9775,#8042,#8043);
#6494=AXIS2_PLACEMENT_3D('',#9779,#8045,#8046);
#6495=AXIS2_PLACEMENT_3D('',#9781,#8048,#8049);
#6496=AXIS2_PLACEMENT_3D('',#9786,#8051,#8052);
#6497=AXIS2_PLACEMENT_3D('',#9789,#8054,#8055);
#6498=AXIS2_PLACEMENT_3D('',#9790,#8056,#8057);
#6499=AXIS2_PLACEMENT_3D('',#9794,#8059,#8060);
#6500=AXIS2_PLACEMENT_3D('',#9796,#8062,#8063);
#6501=AXIS2_PLACEMENT_3D('',#9799,#8066,#8067);
#6502=AXIS2_PLACEMENT_3D('',#9804,#8070,#8071);
#6503=AXIS2_PLACEMENT_3D('',#9805,#8072,#8073);
#6504=AXIS2_PLACEMENT_3D('',#9810,#8076,#8077);
#6505=AXIS2_PLACEMENT_3D('',#9811,#8078,#8079);
#6506=AXIS2_PLACEMENT_3D('',#9814,#8082,#8083);
#6507=AXIS2_PLACEMENT_3D('',#9819,#8086,#8087);
#6508=AXIS2_PLACEMENT_3D('',#9820,#8088,#8089);
#6509=AXIS2_PLACEMENT_3D('',#9825,#8092,#8093);
#6510=AXIS2_PLACEMENT_3D('',#9826,#8094,#8095);
#6511=AXIS2_PLACEMENT_3D('',#9829,#8098,#8099);
#6512=AXIS2_PLACEMENT_3D('',#9835,#8103,#8104);
#6513=AXIS2_PLACEMENT_3D('',#9839,#8107,#8108);
#6514=AXIS2_PLACEMENT_3D('',#9843,#8111,#8112);
#6515=AXIS2_PLACEMENT_3D('',#9847,#8115,#8116);
#6516=AXIS2_PLACEMENT_3D('',#9851,#8119,#8120);
#6517=AXIS2_PLACEMENT_3D('',#9855,#8123,#8124);
#6518=AXIS2_PLACEMENT_3D('',#9856,#8125,#8126);
#6519=AXIS2_PLACEMENT_3D('',#9861,#8128,#8129);
#6520=AXIS2_PLACEMENT_3D('',#9864,#8131,#8132);
#6521=AXIS2_PLACEMENT_3D('',#9865,#8133,#8134);
#6522=AXIS2_PLACEMENT_3D('',#9869,#8136,#8137);
#6523=AXIS2_PLACEMENT_3D('',#9871,#8139,#8140);
#6524=AXIS2_PLACEMENT_3D('',#9875,#8142,#8143);
#6525=AXIS2_PLACEMENT_3D('',#9877,#8145,#8146);
#6526=AXIS2_PLACEMENT_3D('',#9881,#8148,#8149);
#6527=AXIS2_PLACEMENT_3D('',#9883,#8151,#8152);
#6528=AXIS2_PLACEMENT_3D('',#9886,#8154,#8155);
#6529=AXIS2_PLACEMENT_3D('',#9888,#8157,#8158);
#6530=AXIS2_PLACEMENT_3D('',#9891,#8160,#8161);
#6531=AXIS2_PLACEMENT_3D('',#9892,#8162,#8163);
#6532=AXIS2_PLACEMENT_3D('',#9895,#8165,#8166);
#6533=AXIS2_PLACEMENT_3D('',#9896,#8167,#8168);
#6534=AXIS2_PLACEMENT_3D('',#9899,#8170,#8171);
#6535=AXIS2_PLACEMENT_3D('',#9900,#8172,#8173);
#6536=AXIS2_PLACEMENT_3D('',#9903,#8175,#8176);
#6537=AXIS2_PLACEMENT_3D('',#9904,#8177,#8178);
#6538=AXIS2_PLACEMENT_3D('',#9907,#8180,#8181);
#6539=AXIS2_PLACEMENT_3D('',#9908,#8182,#8183);
#6540=AXIS2_PLACEMENT_3D('',#9911,#8185,#8186);
#6541=AXIS2_PLACEMENT_3D('',#9912,#8187,#8188);
#6542=AXIS2_PLACEMENT_3D('',#9915,#8191,#8192);
#6543=AXIS2_PLACEMENT_3D('',#9917,#8194,#8195);
#6544=AXIS2_PLACEMENT_3D('',#9919,#8197,#8198);
#6545=AXIS2_PLACEMENT_3D('',#9920,#8199,#8200);
#6546=AXIS2_PLACEMENT_3D('',#9922,#8202,#8203);
#6547=AXIS2_PLACEMENT_3D('',#9924,#8205,#8206);
#6548=AXIS2_PLACEMENT_3D('',#9926,#8208,#8209);
#7996=DIRECTION('axis',(0.,0.,1.));
#7997=DIRECTION('refdir',(1.,0.,0.));
#7998=DIRECTION('center_axis',(0.,0.,-1.));
#7999=DIRECTION('ref_axis',(-1.,0.,0.));
#8000=DIRECTION('center_axis',(0.,0.,-1.));
#8001=DIRECTION('ref_axis',(-1.,0.,0.));
#8002=DIRECTION('',(0.,0.,-1.));
#8003=DIRECTION('center_axis',(0.,0.,1.));
#8004=DIRECTION('ref_axis',(-1.,0.,0.));
#8005=DIRECTION('center_axis',(0.,0.,-1.));
#8006=DIRECTION('ref_axis',(-1.,0.,0.));
#8007=DIRECTION('center_axis',(0.,0.,-1.));
#8008=DIRECTION('ref_axis',(-1.,0.,0.));
#8009=DIRECTION('',(0.,0.,-1.));
#8010=DIRECTION('center_axis',(0.,0.,1.));
#8011=DIRECTION('ref_axis',(-1.,0.,0.));
#8012=DIRECTION('center_axis',(0.,0.,-1.));
#8013=DIRECTION('ref_axis',(-1.,0.,0.));
#8014=DIRECTION('center_axis',(0.,0.,-1.));
#8015=DIRECTION('ref_axis',(-1.,0.,0.));
#8016=DIRECTION('',(0.,0.,-1.));
#8017=DIRECTION('center_axis',(0.,0.,1.));
#8018=DIRECTION('ref_axis',(-1.,0.,0.));
#8019=DIRECTION('center_axis',(0.,0.,-1.));
#8020=DIRECTION('ref_axis',(-1.,0.,0.));
#8021=DIRECTION('center_axis',(0.,0.,-1.));
#8022=DIRECTION('ref_axis',(-1.,0.,0.));
#8023=DIRECTION('',(0.,0.,-1.));
#8024=DIRECTION('center_axis',(0.,0.,1.));
#8025=DIRECTION('ref_axis',(-1.,0.,0.));
#8026=DIRECTION('center_axis',(-1.,0.,0.));
#8027=DIRECTION('ref_axis',(0.,-0.707106781186548,-0.707106781186548));
#8028=DIRECTION('',(1.,0.,0.));
#8029=DIRECTION('center_axis',(-0.923879532511283,-0.382683432365099,4.10284931589583E-15));
#8030=DIRECTION('ref_axis',(0.382683432365098,-0.923879532511283,9.90515446280861E-15));
#8031=DIRECTION('',(-1.,0.,0.));
#8032=DIRECTION('center_axis',(-0.923879532511286,0.382683432365092,0.));
#8033=DIRECTION('ref_axis',(0.382683432365091,0.923879532511286,0.));
#8034=DIRECTION('center_axis',(0.,1.,0.));
#8035=DIRECTION('ref_axis',(0.707106781186551,0.,-0.707106781186544));
#8036=DIRECTION('',(0.,1.,0.));
#8037=DIRECTION('center_axis',(-0.382683432365083,-0.92387953251129,0.));
#8038=DIRECTION('ref_axis',(0.923879532511289,-0.382683432365083,0.));
#8039=DIRECTION('',(0.,-1.,0.));
#8040=DIRECTION('center_axis',(0.382683432365097,0.923879532511284,8.49727915508632E-16));
#8041=DIRECTION('ref_axis',(0.923879532511284,-0.382683432365097,2.05142465794791E-15));
#8042=DIRECTION('center_axis',(0.707106781186548,0.707106781186548,0.));
#8043=DIRECTION('ref_axis',(0.499999999999996,-0.500000000000002,-0.707106781186549));
#8044=DIRECTION('',(0.707106781186548,0.707106781186548,0.));
#8045=DIRECTION('center_axis',(-0.92387953251129,-0.382683432365082,0.));
#8046=DIRECTION('ref_axis',(0.382683432365082,-0.92387953251129,0.));
#8047=DIRECTION('',(-0.707106781186548,-0.707106781186548,0.));
#8048=DIRECTION('center_axis',(0.,1.,0.));
#8049=DIRECTION('ref_axis',(0.707106781186548,0.,-0.707106781186548));
#8050=DIRECTION('',(0.,-1.,0.));
#8051=DIRECTION('center_axis',(0.382683432365093,0.923879532511285,0.));
#8052=DIRECTION('ref_axis',(0.923879532511285,-0.382683432365093,0.));
#8053=DIRECTION('',(0.,1.,0.));
#8054=DIRECTION('center_axis',(0.382683432365092,-0.923879532511286,0.));
#8055=DIRECTION('ref_axis',(-0.923879532511286,-0.382683432365092,0.));
#8056=DIRECTION('center_axis',(1.,4.56509835347174E-16,0.));
#8057=DIRECTION('ref_axis',(0.,-0.707106781186551,-0.707106781186544));
#8058=DIRECTION('',(1.,4.56509835347174E-16,0.));
#8059=DIRECTION('center_axis',(-0.923879532511287,-0.38268343236509,0.));
#8060=DIRECTION('ref_axis',(-0.38268343236509,0.923879532511287,0.));
#8061=DIRECTION('',(-1.,-4.56509835347174E-16,0.));
#8062=DIRECTION('center_axis',(0.707106781186548,0.707106781186547,0.));
#8063=DIRECTION('ref_axis',(0.5,-0.5,-0.707106781186547));
#8064=DIRECTION('',(-0.707106781186548,-0.707106781186547,0.));
#8065=DIRECTION('',(0.707106781186548,0.707106781186547,0.));
#8066=DIRECTION('center_axis',(-0.707106781186548,0.707106781186548,0.));
#8067=DIRECTION('ref_axis',(0.5,0.5,-0.707106781186547));
#8068=DIRECTION('',(0.707106781186548,-0.707106781186548,0.));
#8069=DIRECTION('',(-0.707106781186548,0.707106781186548,0.));
#8070=DIRECTION('center_axis',(0.923879532511286,-0.382683432365092,0.));
#8071=DIRECTION('ref_axis',(-0.382683432365091,-0.923879532511286,0.));
#8072=DIRECTION('center_axis',(-1.,0.,0.));
#8073=DIRECTION('ref_axis',(0.,0.707106781186548,-0.707106781186548));
#8074=DIRECTION('',(1.,0.,0.));
#8075=DIRECTION('',(-1.,0.,0.));
#8076=DIRECTION('center_axis',(0.923879532511286,0.382683432365092,0.));
#8077=DIRECTION('ref_axis',(0.382683432365092,-0.923879532511286,0.));
#8078=DIRECTION('center_axis',(0.707106781186548,0.707106781186548,0.));
#8079=DIRECTION('ref_axis',(0.5,-0.5,-0.707106781186547));
#8080=DIRECTION('',(0.707106781186548,0.707106781186548,0.));
#8081=DIRECTION('',(-0.707106781186548,-0.707106781186548,0.));
#8082=DIRECTION('center_axis',(-0.707106781186548,-0.707106781186548,0.));
#8083=DIRECTION('ref_axis',(-0.5,0.5,-0.707106781186547));
#8084=DIRECTION('',(0.707106781186548,0.707106781186548,0.));
#8085=DIRECTION('',(-0.707106781186548,-0.707106781186548,0.));
#8086=DIRECTION('center_axis',(0.382683432365092,0.923879532511286,0.));
#8087=DIRECTION('ref_axis',(0.923879532511286,-0.382683432365091,0.));
#8088=DIRECTION('center_axis',(0.,-1.,0.));
#8089=DIRECTION('ref_axis',(-0.707106781186548,0.,-0.707106781186548));
#8090=DIRECTION('',(0.,1.,0.));
#8091=DIRECTION('',(0.,-1.,0.));
#8092=DIRECTION('center_axis',(-0.382683432365092,0.923879532511286,0.));
#8093=DIRECTION('ref_axis',(0.923879532511286,0.382683432365092,0.));
#8094=DIRECTION('center_axis',(0.707106781186548,-0.707106781186548,0.));
#8095=DIRECTION('ref_axis',(-0.5,-0.5,-0.707106781186547));
#8096=DIRECTION('',(-0.707106781186548,0.707106781186548,0.));
#8097=DIRECTION('',(0.707106781186548,-0.707106781186548,0.));
#8098=DIRECTION('center_axis',(0.707106781186548,-0.707106781186548,0.));
#8099=DIRECTION('ref_axis',(0.,0.,-1.));
#8100=DIRECTION('',(0.,0.,1.));
#8101=DIRECTION('',(0.707106781186548,0.707106781186548,0.));
#8102=DIRECTION('',(0.,0.,-1.));
#8103=DIRECTION('center_axis',(1.,0.,0.));
#8104=DIRECTION('ref_axis',(0.,1.,0.));
#8105=DIRECTION('',(0.,0.,1.));
#8106=DIRECTION('',(0.,1.,0.));
#8107=DIRECTION('center_axis',(0.707106781186548,-0.707106781186548,0.));
#8108=DIRECTION('ref_axis',(0.707106781186548,0.707106781186548,0.));
#8109=DIRECTION('',(0.,0.,1.));
#8110=DIRECTION('',(0.707106781186548,0.707106781186548,0.));
#8111=DIRECTION('center_axis',(4.56509835347174E-16,-1.,0.));
#8112=DIRECTION('ref_axis',(1.,4.56509835347174E-16,0.));
#8113=DIRECTION('',(0.,0.,-1.));
#8114=DIRECTION('',(1.,4.56509835347174E-16,0.));
#8115=DIRECTION('center_axis',(0.707106781186547,-0.707106781186548,0.));
#8116=DIRECTION('ref_axis',(0.,0.,-1.));
#8117=DIRECTION('',(0.,0.,1.));
#8118=DIRECTION('',(0.707106781186548,0.707106781186547,0.));
#8119=DIRECTION('center_axis',(1.,0.,0.));
#8120=DIRECTION('ref_axis',(0.,1.,0.));
#8121=DIRECTION('',(0.,0.,1.));
#8122=DIRECTION('',(0.,1.,0.));
#8123=DIRECTION('center_axis',(0.,0.,1.));
#8124=DIRECTION('ref_axis',(1.,0.,0.));
#8125=DIRECTION('center_axis',(0.707106781186548,-0.707106781186548,0.));
#8126=DIRECTION('ref_axis',(-0.500000000000005,-0.500000000000005,0.707106781186541));
#8127=DIRECTION('',(-0.707106781186548,0.707106781186548,0.));
#8128=DIRECTION('center_axis',(0.382683432365092,-0.923879532511286,0.));
#8129=DIRECTION('ref_axis',(-0.923879532511286,-0.382683432365092,0.));
#8130=DIRECTION('',(0.707106781186548,-0.707106781186548,0.));
#8131=DIRECTION('center_axis',(0.923879532511286,-0.382683432365092,0.));
#8132=DIRECTION('ref_axis',(-0.382683432365092,-0.923879532511286,0.));
#8133=DIRECTION('center_axis',(0.,-1.,0.));
#8134=DIRECTION('ref_axis',(-0.707106781186554,0.,0.707106781186541));
#8135=DIRECTION('',(0.,1.,0.));
#8136=DIRECTION('center_axis',(-0.382683432365092,-0.923879532511286,0.));
#8137=DIRECTION('ref_axis',(-0.923879532511286,0.382683432365092,0.));
#8138=DIRECTION('',(0.,-1.,0.));
#8139=DIRECTION('center_axis',(-0.707106781186548,-0.707106781186548,0.));
#8140=DIRECTION('ref_axis',(-0.500000000000005,0.500000000000005,0.707106781186541));
#8141=DIRECTION('',(0.707106781186548,0.707106781186548,0.));
#8142=DIRECTION('center_axis',(-0.923879532511286,-0.382683432365092,0.));
#8143=DIRECTION('ref_axis',(-0.382683432365092,0.923879532511286,0.));
#8144=DIRECTION('',(-0.707106781186548,-0.707106781186548,0.));
#8145=DIRECTION('center_axis',(-1.,0.,0.));
#8146=DIRECTION('ref_axis',(0.,0.707106781186554,0.707106781186541));
#8147=DIRECTION('',(1.,0.,0.));
#8148=DIRECTION('center_axis',(-0.923879532511286,0.382683432365092,0.));
#8149=DIRECTION('ref_axis',(0.382683432365092,0.923879532511286,0.));
#8150=DIRECTION('',(-1.,0.,0.));
#8151=DIRECTION('center_axis',(-0.707106781186548,0.707106781186548,0.));
#8152=DIRECTION('ref_axis',(0.500000000000005,0.500000000000005,0.707106781186541));
#8153=DIRECTION('',(0.707106781186548,-0.707106781186548,0.));
#8154=DIRECTION('center_axis',(-0.382683432365092,0.923879532511286,0.));
#8155=DIRECTION('ref_axis',(0.923879532511286,0.382683432365092,0.));
#8156=DIRECTION('',(-0.707106781186548,0.707106781186548,0.));
#8157=DIRECTION('center_axis',(0.,1.,0.));
#8158=DIRECTION('ref_axis',(0.707106781186554,0.,0.707106781186541));
#8159=DIRECTION('',(0.,-1.,0.));
#8160=DIRECTION('center_axis',(0.382683432365093,0.923879532511285,0.));
#8161=DIRECTION('ref_axis',(0.923879532511285,-0.382683432365093,0.));
#8162=DIRECTION('center_axis',(-0.707106781186548,-0.707106781186547,0.));
#8163=DIRECTION('ref_axis',(0.5,-0.5,0.707106781186547));
#8164=DIRECTION('',(-0.707106781186548,-0.707106781186547,0.));
#8165=DIRECTION('center_axis',(0.923879532511287,0.38268343236509,0.));
#8166=DIRECTION('ref_axis',(-0.38268343236509,0.923879532511287,0.));
#8167=DIRECTION('center_axis',(1.,4.56509835347174E-16,0.));
#8168=DIRECTION('ref_axis',(0.,-0.707106781186557,0.707106781186538));
#8169=DIRECTION('',(-1.,-4.56509835347174E-16,0.));
#8170=DIRECTION('center_axis',(0.92387953251129,0.382683432365082,0.));
#8171=DIRECTION('ref_axis',(-0.382683432365082,0.92387953251129,0.));
#8172=DIRECTION('center_axis',(0.707106781186548,0.707106781186548,0.));
#8173=DIRECTION('ref_axis',(0.500000000000005,-0.500000000000005,0.707106781186541));
#8174=DIRECTION('',(-0.707106781186548,-0.707106781186548,0.));
#8175=DIRECTION('center_axis',(0.382683432365087,0.923879532511288,0.));
#8176=DIRECTION('ref_axis',(-0.923879532511288,0.382683432365087,0.));
#8177=DIRECTION('center_axis',(0.,1.,0.));
#8178=DIRECTION('ref_axis',(0.707106781186557,0.,0.707106781186538));
#8179=DIRECTION('',(0.,-1.,0.));
#8180=DIRECTION('center_axis',(0.382683432365097,0.923879532511284,-8.4972791550864E-16));
#8181=DIRECTION('ref_axis',(0.923879532511284,-0.382683432365097,-2.05142465794793E-15));
#8182=DIRECTION('center_axis',(-0.707106781186548,-0.707106781186548,0.));
#8183=DIRECTION('ref_axis',(0.5,-0.5,0.707106781186547));
#8184=DIRECTION('',(-0.707106781186548,-0.707106781186548,0.));
#8185=DIRECTION('center_axis',(0.923879532511283,0.382683432365099,0.));
#8186=DIRECTION('ref_axis',(-0.382683432365099,0.923879532511283,0.));
#8187=DIRECTION('center_axis',(1.,0.,0.));
#8188=DIRECTION('ref_axis',(0.,-0.707106781186554,0.707106781186541));
#8189=DIRECTION('',(1.,0.,0.));
#8190=DIRECTION('',(-1.,0.,0.));
#8191=DIRECTION('center_axis',(0.,-1.,0.));
#8192=DIRECTION('ref_axis',(1.,0.,0.));
#8193=DIRECTION('',(0.,0.,1.));
#8194=DIRECTION('center_axis',(-0.707106781186548,-0.707106781186548,0.));
#8195=DIRECTION('ref_axis',(0.707106781186548,-0.707106781186548,0.));
#8196=DIRECTION('',(0.,0.,1.));
#8197=DIRECTION('center_axis',(0.,0.,1.));
#8198=DIRECTION('ref_axis',(1.,0.,0.));
#8199=DIRECTION('center_axis',(-1.,0.,0.));
#8200=DIRECTION('ref_axis',(0.,-1.,0.));
#8201=DIRECTION('',(0.,0.,1.));
#8202=DIRECTION('center_axis',(-0.707106781186548,0.707106781186548,0.));
#8203=DIRECTION('ref_axis',(-0.707106781186548,-0.707106781186548,0.));
#8204=DIRECTION('',(0.,0.,1.));
#8205=DIRECTION('center_axis',(0.,1.,0.));
#8206=DIRECTION('ref_axis',(-1.,0.,0.));
#8207=DIRECTION('',(0.,0.,1.));
#8208=DIRECTION('center_axis',(0.707106781186548,0.707106781186548,0.));
#8209=DIRECTION('ref_axis',(-0.707106781186548,0.707106781186548,0.));
#9732=CARTESIAN_POINT('',(0.,0.,0.));
#9733=CARTESIAN_POINT('Origin',(-32.4855257306532,-32.7240321735238,86.));
#9734=CARTESIAN_POINT('',(-29.4855257306532,-32.7240321735238,74.));
#9735=CARTESIAN_POINT('Origin',(-32.4855257306532,-32.7240321735238,74.));
#9736=CARTESIAN_POINT('',(-29.4855257306532,-32.7240321735238,62.));
#9737=CARTESIAN_POINT('',(-29.4855257306532,-32.7240321735238,86.));
#9738=CARTESIAN_POINT('Origin',(-32.4855257306532,-32.7240321735238,62.));
#9739=CARTESIAN_POINT('Origin',(32.5144742693468,32.2759678264762,86.));
#9740=CARTESIAN_POINT('',(35.5144742693468,32.2759678264762,74.));
#9741=CARTESIAN_POINT('Origin',(32.5144742693468,32.2759678264762,74.));
#9742=CARTESIAN_POINT('',(35.5144742693468,32.2759678264762,62.));
#9743=CARTESIAN_POINT('',(35.5144742693468,32.2759678264762,86.));
#9744=CARTESIAN_POINT('Origin',(32.5144742693468,32.2759678264762,62.));
#9745=CARTESIAN_POINT('Origin',(-32.4855257306532,32.2759678264762,86.));
#9746=CARTESIAN_POINT('',(-29.4855257306532,32.2759678264762,74.));
#9747=CARTESIAN_POINT('Origin',(-32.4855257306532,32.2759678264762,74.));
#9748=CARTESIAN_POINT('',(-29.4855257306532,32.2759678264762,62.));
#9749=CARTESIAN_POINT('',(-29.4855257306532,32.2759678264762,86.));
#9750=CARTESIAN_POINT('Origin',(-32.4855257306532,32.2759678264762,62.));
#9751=CARTESIAN_POINT('Origin',(32.5144742693468,-7.72403217352376,86.));
#9752=CARTESIAN_POINT('',(35.5144742693468,-7.72403217352376,74.));
#9753=CARTESIAN_POINT('Origin',(32.5144742693468,-7.72403217352376,74.));
#9754=CARTESIAN_POINT('',(35.5144742693468,-7.72403217352376,62.));
#9755=CARTESIAN_POINT('',(35.5144742693468,-7.72403217352376,86.));
#9756=CARTESIAN_POINT('Origin',(32.5144742693468,-7.72403217352376,62.));
#9757=CARTESIAN_POINT('Origin',(-22.5,-49.,63.));
#9758=CARTESIAN_POINT('',(-44.5857864376269,-49.,62.));
#9759=CARTESIAN_POINT('',(15.5857864376269,-49.,62.));
#9760=CARTESIAN_POINT('',(-22.5,-49.,62.));
#9761=CARTESIAN_POINT('',(16.,-50.,63.));
#9762=CARTESIAN_POINT('Origin',(15.5857864376269,-49.,63.));
#9763=CARTESIAN_POINT('',(-45.,-50.,63.));
#9764=CARTESIAN_POINT('',(-22.5,-50.,63.));
#9765=CARTESIAN_POINT('Origin',(-44.5857864376269,-49.,63.));
#9766=CARTESIAN_POINT('Origin',(20.,-25.,63.));
#9767=CARTESIAN_POINT('',(20.,-44.5857864376269,62.));
#9768=CARTESIAN_POINT('',(20.,-30.8578643762691,62.));
#9769=CARTESIAN_POINT('',(20.,-25.,62.));
#9770=CARTESIAN_POINT('',(21.,-31.2720779386421,63.));
#9771=CARTESIAN_POINT('Origin',(20.,-30.8578643762691,63.));
#9772=CARTESIAN_POINT('',(21.,-45.,63.));
#9773=CARTESIAN_POINT('',(21.,-25.,63.));
#9774=CARTESIAN_POINT('Origin',(20.,-44.5857864376269,63.));
#9775=CARTESIAN_POINT('Origin',(22.860912703474,-27.9969516727951,63.));
#9776=CARTESIAN_POINT('',(30.857864376269,-20.,62.));
#9777=CARTESIAN_POINT('',(22.860912703474,-27.9969516727951,62.));
#9778=CARTESIAN_POINT('',(31.2720779386421,-21.,63.));
#9779=CARTESIAN_POINT('Origin',(30.857864376269,-20.,63.));
#9780=CARTESIAN_POINT('',(23.5680194846605,-28.7040584539816,63.));
#9781=CARTESIAN_POINT('Origin',(49.,-10.5,63.));
#9782=CARTESIAN_POINT('',(50.,45.,63.));
#9783=CARTESIAN_POINT('',(50.,-16.,63.));
#9784=CARTESIAN_POINT('',(50.,-10.5,63.));
#9785=CARTESIAN_POINT('',(49.,-15.5857864376269,62.));
#9786=CARTESIAN_POINT('Origin',(49.,-15.5857864376269,63.));
#9787=CARTESIAN_POINT('',(49.,44.5857864376269,62.));
#9788=CARTESIAN_POINT('',(49.,-10.5,62.));
#9789=CARTESIAN_POINT('Origin',(49.,44.5857864376269,63.));
#9790=CARTESIAN_POINT('Origin',(15.6360389693211,-20.,63.));
#9791=CARTESIAN_POINT('',(44.5857864376269,-20.,62.));
#9792=CARTESIAN_POINT('',(15.6360389693211,-20.,62.));
#9793=CARTESIAN_POINT('',(45.,-21.,63.));
#9794=CARTESIAN_POINT('Origin',(44.5857864376269,-20.,63.));
#9795=CARTESIAN_POINT('',(15.6360389693211,-21.,63.));
#9796=CARTESIAN_POINT('Origin',(39.5428932188134,-25.0428932188135,63.));
#9797=CARTESIAN_POINT('',(40.25,-25.75,63.));
#9798=CARTESIAN_POINT('',(39.5428932188134,-25.0428932188135,62.));
#9799=CARTESIAN_POINT('Origin',(48.0428932188135,45.5428932188135,63.));
#9800=CARTESIAN_POINT('',(45.,50.,63.));
#9801=CARTESIAN_POINT('',(48.75,46.25,63.));
#9802=CARTESIAN_POINT('',(44.5857864376269,49.,62.));
#9803=CARTESIAN_POINT('',(48.0428932188135,45.5428932188135,62.));
#9804=CARTESIAN_POINT('Origin',(44.5857864376269,49.,63.));
#9805=CARTESIAN_POINT('Origin',(22.5,49.,63.));
#9806=CARTESIAN_POINT('',(-45.,50.,63.));
#9807=CARTESIAN_POINT('',(22.5,50.,63.));
#9808=CARTESIAN_POINT('',(-44.5857864376269,49.,62.));
#9809=CARTESIAN_POINT('',(22.5,49.,62.));
#9810=CARTESIAN_POINT('Origin',(-44.5857864376269,49.,63.));
#9811=CARTESIAN_POINT('Origin',(25.0428932188134,-39.5428932188134,63.));
#9812=CARTESIAN_POINT('',(25.0428932188134,-39.5428932188134,62.));
#9813=CARTESIAN_POINT('',(25.75,-40.25,63.));
#9814=CARTESIAN_POINT('Origin',(-45.5428932188135,48.0428932188135,63.));
#9815=CARTESIAN_POINT('',(-50.,45.,63.));
#9816=CARTESIAN_POINT('',(-46.25,48.75,63.));
#9817=CARTESIAN_POINT('',(-49.,44.5857864376269,62.));
#9818=CARTESIAN_POINT('',(-45.5428932188135,48.0428932188135,62.));
#9819=CARTESIAN_POINT('Origin',(-49.,44.5857864376269,63.));
#9820=CARTESIAN_POINT('Origin',(-49.,22.5,63.));
#9821=CARTESIAN_POINT('',(-50.,-45.,63.));
#9822=CARTESIAN_POINT('',(-50.,22.5,63.));
#9823=CARTESIAN_POINT('',(-49.,-44.5857864376269,62.));
#9824=CARTESIAN_POINT('',(-49.,22.5,62.));
#9825=CARTESIAN_POINT('Origin',(-49.,-44.5857864376269,63.));
#9826=CARTESIAN_POINT('Origin',(-48.0428932188135,-45.5428932188135,63.));
#9827=CARTESIAN_POINT('',(-48.75,-46.25,63.));
#9828=CARTESIAN_POINT('',(-48.0428932188135,-45.5428932188135,62.));
#9829=CARTESIAN_POINT('Origin',(18.5,-47.5,62.));
#9830=CARTESIAN_POINT('',(21.,-45.,73.));
#9831=CARTESIAN_POINT('',(21.,-45.,62.));
#9832=CARTESIAN_POINT('',(16.,-50.,73.));
#9833=CARTESIAN_POINT('',(25.75,-40.25,73.));
#9834=CARTESIAN_POINT('',(16.,-50.,62.));
#9835=CARTESIAN_POINT('Origin',(21.,-50.,62.));
#9836=CARTESIAN_POINT('',(21.,-31.2720779386421,73.));
#9837=CARTESIAN_POINT('',(21.,-31.2720779386421,62.));
#9838=CARTESIAN_POINT('',(21.,-25.,73.));
#9839=CARTESIAN_POINT('Origin',(21.,-31.2720779386421,62.));
#9840=CARTESIAN_POINT('',(31.2720779386421,-21.,73.));
#9841=CARTESIAN_POINT('',(31.2720779386421,-21.,62.));
#9842=CARTESIAN_POINT('',(23.5680194846605,-28.7040584539816,73.));
#9843=CARTESIAN_POINT('Origin',(31.2720779386421,-21.,62.));
#9844=CARTESIAN_POINT('',(45.,-21.,73.));
#9845=CARTESIAN_POINT('',(45.,-21.,62.));
#9846=CARTESIAN_POINT('',(15.6360389693211,-21.,73.));
#9847=CARTESIAN_POINT('Origin',(47.5,-18.5,62.));
#9848=CARTESIAN_POINT('',(50.,-16.,73.));
#9849=CARTESIAN_POINT('',(50.,-16.,62.));
#9850=CARTESIAN_POINT('',(40.25,-25.75,73.));
#9851=CARTESIAN_POINT('Origin',(50.,-21.,62.));
#9852=CARTESIAN_POINT('',(50.,45.,73.));
#9853=CARTESIAN_POINT('',(50.,45.,62.));
#9854=CARTESIAN_POINT('',(50.,-10.5,73.));
#9855=CARTESIAN_POINT('Origin',(0.,0.,62.));
#9856=CARTESIAN_POINT('Origin',(-48.0428932188135,-45.5428932188135,73.));
#9857=CARTESIAN_POINT('',(-44.5857864376269,-49.,74.));
#9858=CARTESIAN_POINT('',(-49.,-44.5857864376269,74.));
#9859=CARTESIAN_POINT('',(-48.0428932188135,-45.5428932188135,74.));
#9860=CARTESIAN_POINT('',(-50.,-45.,73.));
#9861=CARTESIAN_POINT('Origin',(-49.,-44.5857864376269,73.));
#9862=CARTESIAN_POINT('',(-45.,-50.,73.));
#9863=CARTESIAN_POINT('',(-48.75,-46.25,73.));
#9864=CARTESIAN_POINT('Origin',(-44.5857864376269,-49.,73.));
#9865=CARTESIAN_POINT('Origin',(-49.,22.5,73.));
#9866=CARTESIAN_POINT('',(-49.,44.5857864376269,74.));
#9867=CARTESIAN_POINT('',(-49.,22.5,74.));
#9868=CARTESIAN_POINT('',(-50.,45.,73.));
#9869=CARTESIAN_POINT('Origin',(-49.,44.5857864376269,73.));
#9870=CARTESIAN_POINT('',(-50.,22.5,73.));
#9871=CARTESIAN_POINT('Origin',(-45.5428932188135,48.0428932188135,73.));
#9872=CARTESIAN_POINT('',(-44.5857864376269,49.,74.));
#9873=CARTESIAN_POINT('',(-45.5428932188135,48.0428932188135,74.));
#9874=CARTESIAN_POINT('',(-45.,50.,73.));
#9875=CARTESIAN_POINT('Origin',(-44.5857864376269,49.,73.));
#9876=CARTESIAN_POINT('',(-46.25,48.75,73.));
#9877=CARTESIAN_POINT('Origin',(22.5,49.,73.));
#9878=CARTESIAN_POINT('',(44.5857864376269,49.,74.));
#9879=CARTESIAN_POINT('',(22.5,49.,74.));
#9880=CARTESIAN_POINT('',(45.,50.,73.));
#9881=CARTESIAN_POINT('Origin',(44.5857864376269,49.,73.));
#9882=CARTESIAN_POINT('',(22.5,50.,73.));
#9883=CARTESIAN_POINT('Origin',(48.0428932188135,45.5428932188135,73.));
#9884=CARTESIAN_POINT('',(49.,44.5857864376269,74.));
#9885=CARTESIAN_POINT('',(48.0428932188135,45.5428932188135,74.));
#9886=CARTESIAN_POINT('Origin',(49.,44.5857864376269,73.));
#9887=CARTESIAN_POINT('',(48.75,46.25,73.));
#9888=CARTESIAN_POINT('Origin',(49.,-10.5,73.));
#9889=CARTESIAN_POINT('',(49.,-15.5857864376269,74.));
#9890=CARTESIAN_POINT('',(49.,-10.5,74.));
#9891=CARTESIAN_POINT('Origin',(49.,-15.5857864376269,73.));
#9892=CARTESIAN_POINT('Origin',(39.5428932188134,-25.0428932188135,73.));
#9893=CARTESIAN_POINT('',(44.5857864376269,-20.,74.));
#9894=CARTESIAN_POINT('',(39.5428932188134,-25.0428932188135,74.));
#9895=CARTESIAN_POINT('Origin',(44.5857864376269,-20.,73.));
#9896=CARTESIAN_POINT('Origin',(15.6360389693211,-20.,73.));
#9897=CARTESIAN_POINT('',(30.857864376269,-20.,74.));
#9898=CARTESIAN_POINT('',(15.6360389693211,-20.,74.));
#9899=CARTESIAN_POINT('Origin',(30.857864376269,-20.,73.));
#9900=CARTESIAN_POINT('Origin',(22.860912703474,-27.9969516727951,73.));
#9901=CARTESIAN_POINT('',(20.,-30.8578643762691,74.));
#9902=CARTESIAN_POINT('',(22.860912703474,-27.9969516727951,74.));
#9903=CARTESIAN_POINT('Origin',(20.,-30.8578643762691,73.));
#9904=CARTESIAN_POINT('Origin',(20.,-25.,73.));
#9905=CARTESIAN_POINT('',(20.,-44.5857864376269,74.));
#9906=CARTESIAN_POINT('',(20.,-25.,74.));
#9907=CARTESIAN_POINT('Origin',(20.,-44.5857864376269,73.));
#9908=CARTESIAN_POINT('Origin',(25.0428932188134,-39.5428932188134,73.));
#9909=CARTESIAN_POINT('',(15.5857864376269,-49.,74.));
#9910=CARTESIAN_POINT('',(25.0428932188134,-39.5428932188134,74.));
#9911=CARTESIAN_POINT('Origin',(15.5857864376269,-49.,73.));
#9912=CARTESIAN_POINT('Origin',(-22.5,-49.,73.));
#9913=CARTESIAN_POINT('',(-22.5,-50.,73.));
#9914=CARTESIAN_POINT('',(-22.5,-49.,74.));
#9915=CARTESIAN_POINT('Origin',(-45.,-50.,62.));
#9916=CARTESIAN_POINT('',(-45.,-50.,62.));
#9917=CARTESIAN_POINT('Origin',(-50.,-45.,62.));
#9918=CARTESIAN_POINT('',(-50.,-45.,62.));
#9919=CARTESIAN_POINT('Origin',(0.,0.,74.));
#9920=CARTESIAN_POINT('Origin',(-50.,45.,62.));
#9921=CARTESIAN_POINT('',(-50.,45.,62.));
#9922=CARTESIAN_POINT('Origin',(-45.,50.,62.));
#9923=CARTESIAN_POINT('',(-45.,50.,62.));
#9924=CARTESIAN_POINT('Origin',(45.,50.,62.));
#9925=CARTESIAN_POINT('',(45.,50.,62.));
#9926=CARTESIAN_POINT('Origin',(50.,45.,62.));
#10117=UNCERTAINTY_MEASURE_WITH_UNIT(LENGTH_MEASURE(0.01),#10132,
'DISTANCE_ACCURACY_VALUE',
'Maximum model space distance between geometric entities at asserted c
onnectivities');
#10119=UNCERTAINTY_MEASURE_WITH_UNIT(LENGTH_MEASURE(0.01),#10132,
'DISTANCE_ACCURACY_VALUE',
'Maximum model space distance between geometric entities at asserted c
onnectivities');
#10129=(
GEOMETRIC_REPRESENTATION_CONTEXT(3)
GLOBAL_UNCERTAINTY_ASSIGNED_CONTEXT((#10117))
GLOBAL_UNIT_ASSIGNED_CONTEXT((#10132,#10134,#10135))
REPRESENTATION_CONTEXT('','3D')
);
#10131=(
GEOMETRIC_REPRESENTATION_CONTEXT(3)
GLOBAL_UNCERTAINTY_ASSIGNED_CONTEXT((#10119))
GLOBAL_UNIT_ASSIGNED_CONTEXT((#10132,#10134,#10135))
REPRESENTATION_CONTEXT('','3D')
);
#10132=(
LENGTH_UNIT()
NAMED_UNIT(*)
SI_UNIT(.MILLI.,.METRE.)
);
#10134=(
NAMED_UNIT(*)
PLANE_ANGLE_UNIT()
SI_UNIT($,.RADIAN.)
);
#10135=(
NAMED_UNIT(*)
SI_UNIT($,.STERADIAN.)
SOLID_ANGLE_UNIT()
);
#10145=SHAPE_DEFINITION_REPRESENTATION(#10156,#10177);
#10156=PRODUCT_DEFINITION_SHAPE('',$,#10189);
#10177=SHAPE_REPRESENTATION('',(#6474),#10129);
#10179=PRODUCT_DEFINITION_CONTEXT('part definition',#10214,'design');
#10189=PRODUCT_DEFINITION('Middle_Block_02','Middle_Block_02',#10200,#10179);
#10200=PRODUCT_DEFINITION_FORMATION('',$,#10225);
#10214=APPLICATION_CONTEXT(
'Core Data for Automotive Mechanical Design Process');
#10215=PRODUCT_CONTEXT('part definition',#10214,'mechanical');
#10225=PRODUCT('Middle_Block_02','Middle_Block_02',$,(#10215));
#10241=COLOUR_RGB('Dark Blue',0.08,0.2,0.34);
#10242=FILL_AREA_STYLE_COLOUR('',#10241);
#10243=FILL_AREA_STYLE('',(#10242));
#10244=SURFACE_STYLE_FILL_AREA(#10243);
#10245=SURFACE_SIDE_STYLE('',(#10244));
#10246=SURFACE_STYLE_USAGE(.BOTH.,#10245);
#10247=PRESENTATION_STYLE_ASSIGNMENT((#10246));
ENDSEC;
END-ISO-10303-21;
